ISO-10303-21;
HEADER;
/* Generated by software containing ST-Developer
 * from STEP Tools, Inc. (www.steptools.com) 
 */

FILE_DESCRIPTION(
/* description */ ('Spring compression tester'),
/* implementation_level */ '2;1');

FILE_NAME(
/* name */ 'Cap Screw - M5x20.step',
/* time_stamp */ '2026-10-28T03:24:11-07:00',
/* author */ (''),
/* organization */ (''),
/* preprocessor_version */ 'ST-DEVELOPER v20.2',
/* originating_system */ 'Autodesk Translation Framework v15.17.0.0',
/* authorisation */ '');

FILE_SCHEMA (('AUTOMOTIVE_DESIGN { 1 0 10303 214 3 1 1 }'));
ENDSEC;

DATA;
#10=MECHANICAL_DESIGN_GEOMETRIC_PRESENTATION_REPRESENTATION('',(#1155),#43521);
#934=ORIENTED_CLOSED_SHELL('',*,#18596,.F.);
#941=BREP_WITH_VOIDS('Body1',#18595,(#934));
#964=CONICAL_SURFACE('',#20359,0.4,0.785398163397448);
#965=CONICAL_SURFACE('',#20363,0.41,0.785398163397448);
#966=CONICAL_SURFACE('',#20367,0.26,0.463647609000806);
#967=CONICAL_SURFACE('',#20371,0.225,0.785398163397448);
#1020=SHAPE_REPRESENTATION_RELATIONSHIP('SRR','None',#43834,#1080);
#1080=ADVANCED_BREP_SHAPE_REPRESENTATION('',(#941),#43494);
#1155=STYLED_ITEM('',(#44209),#941);
#1473=FACE_BOUND('',#4054,.T.);
#1990=PLANE('',#20357);
#1991=PLANE('',#20365);
#1992=PLANE('',#20373);
#1993=PLANE('',#20374);
#1994=PLANE('',#20375);
#1995=PLANE('',#20376);
#1996=PLANE('',#20377);
#1997=PLANE('',#20378);
#1998=PLANE('',#20379);
#1999=PLANE('',#20380);
#2000=PLANE('',#20381);
#2776=FACE_OUTER_BOUND('',#4049,.T.);
#2777=FACE_OUTER_BOUND('',#4050,.T.);
#2778=FACE_OUTER_BOUND('',#4051,.T.);
#2779=FACE_OUTER_BOUND('',#4052,.T.);
#2780=FACE_OUTER_BOUND('',#4053,.T.);
#2781=FACE_OUTER_BOUND('',#4055,.T.);
#2782=FACE_OUTER_BOUND('',#4056,.T.);
#2783=FACE_OUTER_BOUND('',#4057,.T.);
#2784=FACE_OUTER_BOUND('',#4058,.T.);
#2785=FACE_OUTER_BOUND('',#4059,.T.);
#2786=FACE_OUTER_BOUND('',#4060,.T.);
#2787=FACE_OUTER_BOUND('',#4061,.T.);
#2788=FACE_OUTER_BOUND('',#4062,.T.);
#2789=FACE_OUTER_BOUND('',#4063,.T.);
#2790=FACE_OUTER_BOUND('',#4064,.T.);
#2791=FACE_OUTER_BOUND('',#4065,.T.);
#2792=FACE_OUTER_BOUND('',#4066,.T.);
#4049=EDGE_LOOP('',(#14927));
#4050=EDGE_LOOP('',(#14928,#14929,#14930,#14931));
#4051=EDGE_LOOP('',(#14932,#14933,#14934,#14935));
#4052=EDGE_LOOP('',(#14936,#14937,#14938,#14939));
#4053=EDGE_LOOP('',(#14940));
#4054=EDGE_LOOP('',(#14941));
#4055=EDGE_LOOP('',(#14942,#14943,#14944,#14945));
#4056=EDGE_LOOP('',(#14946,#14947,#14948,#14949));
#4057=EDGE_LOOP('',(#14950,#14951,#14952,#14953));
#4058=EDGE_LOOP('',(#14954));
#4059=EDGE_LOOP('',(#14955,#14956,#14957,#14958));
#4060=EDGE_LOOP('',(#14959,#14960,#14961,#14962));
#4061=EDGE_LOOP('',(#14963,#14964,#14965,#14966));
#4062=EDGE_LOOP('',(#14967,#14968,#14969,#14970));
#4063=EDGE_LOOP('',(#14971,#14972,#14973,#14974));
#4064=EDGE_LOOP('',(#14975,#14976,#14977,#14978));
#4065=EDGE_LOOP('',(#14979,#14980,#14981,#14982,#14983,#14984));
#4066=EDGE_LOOP('',(#14985,#14986,#14987,#14988,#14989,#14990));
#5513=LINE('',#30019,#6945);
#5514=LINE('',#30023,#6946);
#5515=LINE('',#30027,#6947);
#5516=LINE('',#30034,#6948);
#5517=LINE('',#30038,#6949);
#5518=LINE('',#30042,#6950);
#5519=LINE('',#30047,#6951);
#5520=LINE('',#30049,#6952);
#5521=LINE('',#30051,#6953);
#5522=LINE('',#30052,#6954);
#5523=LINE('',#30055,#6955);
#5524=LINE('',#30057,#6956);
#5525=LINE('',#30058,#6957);
#5526=LINE('',#30061,#6958);
#5527=LINE('',#30063,#6959);
#5528=LINE('',#30064,#6960);
#5529=LINE('',#30067,#6961);
#5530=LINE('',#30069,#6962);
#5531=LINE('',#30070,#6963);
#5532=LINE('',#30073,#6964);
#5533=LINE('',#30075,#6965);
#5534=LINE('',#30076,#6966);
#5535=LINE('',#30078,#6967);
#5536=LINE('',#30079,#6968);
#6945=VECTOR('',#24257,0.4);
#6946=VECTOR('',#24262,0.425);
#6947=VECTOR('',#24267,0.41);
#6948=VECTOR('',#24276,0.26);
#6949=VECTOR('',#24281,0.25);
#6950=VECTOR('',#24286,0.225);
#6951=VECTOR('',#24291,1.);
#6952=VECTOR('',#24292,1.);
#6953=VECTOR('',#24293,1.);
#6954=VECTOR('',#24294,1.);
#6955=VECTOR('',#24297,1.);
#6956=VECTOR('',#24298,1.);
#6957=VECTOR('',#24299,1.);
#6958=VECTOR('',#24302,1.);
#6959=VECTOR('',#24303,1.);
#6960=VECTOR('',#24304,1.);
#6961=VECTOR('',#24307,1.);
#6962=VECTOR('',#24308,1.);
#6963=VECTOR('',#24309,1.);
#6964=VECTOR('',#24312,1.);
#6965=VECTOR('',#24313,1.);
#6966=VECTOR('',#24314,1.);
#6967=VECTOR('',#24317,1.);
#6968=VECTOR('',#24318,1.);
#7886=CIRCLE('',#20358,0.375);
#7887=CIRCLE('',#20360,0.425);
#7888=CIRCLE('',#20362,0.425);
#7889=CIRCLE('',#20364,0.395);
#7890=CIRCLE('',#20366,0.27);
#7891=CIRCLE('',#20368,0.24505);
#7892=CIRCLE('',#20370,0.24505);
#7893=CIRCLE('',#20372,0.2);
#9053=VERTEX_POINT('',#30014);
#9054=VERTEX_POINT('',#30017);
#9055=VERTEX_POINT('',#30021);
#9056=VERTEX_POINT('',#30025);
#9057=VERTEX_POINT('',#30029);
#9058=VERTEX_POINT('',#30032);
#9059=VERTEX_POINT('',#30036);
#9060=VERTEX_POINT('',#30040);
#9061=VERTEX_POINT('',#30045);
#9062=VERTEX_POINT('',#30046);
#9063=VERTEX_POINT('',#30048);
#9064=VERTEX_POINT('',#30050);
#9065=VERTEX_POINT('',#30054);
#9066=VERTEX_POINT('',#30056);
#9067=VERTEX_POINT('',#30060);
#9068=VERTEX_POINT('',#30062);
#9069=VERTEX_POINT('',#30066);
#9070=VERTEX_POINT('',#30068);
#9071=VERTEX_POINT('',#30072);
#9072=VERTEX_POINT('',#30074);
#11128=EDGE_CURVE('',#9053,#9053,#7886,.T.);
#11129=EDGE_CURVE('',#9054,#9054,#7887,.T.);
#11130=EDGE_CURVE('',#9054,#9053,#5513,.T.);
#11131=EDGE_CURVE('',#9055,#9055,#7888,.T.);
#11132=EDGE_CURVE('',#9055,#9054,#5514,.T.);
#11133=EDGE_CURVE('',#9056,#9056,#7889,.T.);
#11134=EDGE_CURVE('',#9056,#9055,#5515,.T.);
#11135=EDGE_CURVE('',#9057,#9057,#7890,.T.);
#11136=EDGE_CURVE('',#9058,#9058,#7891,.F.);
#11137=EDGE_CURVE('',#9058,#9057,#5516,.T.);
#11138=EDGE_CURVE('',#9059,#9059,#7892,.F.);
#11139=EDGE_CURVE('',#9059,#9058,#5517,.T.);
#11140=EDGE_CURVE('',#9060,#9060,#7893,.T.);
#11141=EDGE_CURVE('',#9060,#9059,#5518,.T.);
#11142=EDGE_CURVE('',#9061,#9062,#5519,.T.);
#11143=EDGE_CURVE('',#9062,#9063,#5520,.T.);
#11144=EDGE_CURVE('',#9063,#9064,#5521,.T.);
#11145=EDGE_CURVE('',#9061,#9064,#5522,.T.);
#11146=EDGE_CURVE('',#9062,#9065,#5523,.T.);
#11147=EDGE_CURVE('',#9065,#9066,#5524,.T.);
#11148=EDGE_CURVE('',#9066,#9063,#5525,.T.);
#11149=EDGE_CURVE('',#9065,#9067,#5526,.T.);
#11150=EDGE_CURVE('',#9067,#9068,#5527,.T.);
#11151=EDGE_CURVE('',#9068,#9066,#5528,.T.);
#11152=EDGE_CURVE('',#9067,#9069,#5529,.T.);
#11153=EDGE_CURVE('',#9069,#9070,#5530,.T.);
#11154=EDGE_CURVE('',#9070,#9068,#5531,.T.);
#11155=EDGE_CURVE('',#9069,#9071,#5532,.T.);
#11156=EDGE_CURVE('',#9071,#9072,#5533,.T.);
#11157=EDGE_CURVE('',#9072,#9070,#5534,.T.);
#11158=EDGE_CURVE('',#9071,#9061,#5535,.T.);
#11159=EDGE_CURVE('',#9064,#9072,#5536,.T.);
#14927=ORIENTED_EDGE('',*,*,#11128,.F.);
#14928=ORIENTED_EDGE('',*,*,#11129,.F.);
#14929=ORIENTED_EDGE('',*,*,#11130,.T.);
#14930=ORIENTED_EDGE('',*,*,#11128,.T.);
#14931=ORIENTED_EDGE('',*,*,#11130,.F.);
#14932=ORIENTED_EDGE('',*,*,#11131,.F.);
#14933=ORIENTED_EDGE('',*,*,#11132,.T.);
#14934=ORIENTED_EDGE('',*,*,#11129,.T.);
#14935=ORIENTED_EDGE('',*,*,#11132,.F.);
#14936=ORIENTED_EDGE('',*,*,#11133,.F.);
#14937=ORIENTED_EDGE('',*,*,#11134,.T.);
#14938=ORIENTED_EDGE('',*,*,#11131,.T.);
#14939=ORIENTED_EDGE('',*,*,#11134,.F.);
#14940=ORIENTED_EDGE('',*,*,#11133,.T.);
#14941=ORIENTED_EDGE('',*,*,#11135,.F.);
#14942=ORIENTED_EDGE('',*,*,#11136,.F.);
#14943=ORIENTED_EDGE('',*,*,#11137,.T.);
#14944=ORIENTED_EDGE('',*,*,#11135,.T.);
#14945=ORIENTED_EDGE('',*,*,#11137,.F.);
#14946=ORIENTED_EDGE('',*,*,#11138,.F.);
#14947=ORIENTED_EDGE('',*,*,#11139,.T.);
#14948=ORIENTED_EDGE('',*,*,#11136,.T.);
#14949=ORIENTED_EDGE('',*,*,#11139,.F.);
#14950=ORIENTED_EDGE('',*,*,#11140,.F.);
#14951=ORIENTED_EDGE('',*,*,#11141,.T.);
#14952=ORIENTED_EDGE('',*,*,#11138,.T.);
#14953=ORIENTED_EDGE('',*,*,#11141,.F.);
#14954=ORIENTED_EDGE('',*,*,#11140,.T.);
#14955=ORIENTED_EDGE('',*,*,#11142,.T.);
#14956=ORIENTED_EDGE('',*,*,#11143,.T.);
#14957=ORIENTED_EDGE('',*,*,#11144,.T.);
#14958=ORIENTED_EDGE('',*,*,#11145,.F.);
#14959=ORIENTED_EDGE('',*,*,#11146,.T.);
#14960=ORIENTED_EDGE('',*,*,#11147,.T.);
#14961=ORIENTED_EDGE('',*,*,#11148,.T.);
#14962=ORIENTED_EDGE('',*,*,#11143,.F.);
#14963=ORIENTED_EDGE('',*,*,#11149,.T.);
#14964=ORIENTED_EDGE('',*,*,#11150,.T.);
#14965=ORIENTED_EDGE('',*,*,#11151,.T.);
#14966=ORIENTED_EDGE('',*,*,#11147,.F.);
#14967=ORIENTED_EDGE('',*,*,#11152,.T.);
#14968=ORIENTED_EDGE('',*,*,#11153,.T.);
#14969=ORIENTED_EDGE('',*,*,#11154,.T.);
#14970=ORIENTED_EDGE('',*,*,#11150,.F.);
#14971=ORIENTED_EDGE('',*,*,#11155,.T.);
#14972=ORIENTED_EDGE('',*,*,#11156,.T.);
#14973=ORIENTED_EDGE('',*,*,#11157,.T.);
#14974=ORIENTED_EDGE('',*,*,#11153,.F.);
#14975=ORIENTED_EDGE('',*,*,#11158,.T.);
#14976=ORIENTED_EDGE('',*,*,#11145,.T.);
#14977=ORIENTED_EDGE('',*,*,#11159,.T.);
#14978=ORIENTED_EDGE('',*,*,#11156,.F.);
#14979=ORIENTED_EDGE('',*,*,#11158,.F.);
#14980=ORIENTED_EDGE('',*,*,#11155,.F.);
#14981=ORIENTED_EDGE('',*,*,#11152,.F.);
#14982=ORIENTED_EDGE('',*,*,#11149,.F.);
#14983=ORIENTED_EDGE('',*,*,#11146,.F.);
#14984=ORIENTED_EDGE('',*,*,#11142,.F.);
#14985=ORIENTED_EDGE('',*,*,#11159,.F.);
#14986=ORIENTED_EDGE('',*,*,#11144,.F.);
#14987=ORIENTED_EDGE('',*,*,#11148,.F.);
#14988=ORIENTED_EDGE('',*,*,#11151,.F.);
#14989=ORIENTED_EDGE('',*,*,#11154,.F.);
#14990=ORIENTED_EDGE('',*,*,#11157,.F.);
#17257=CYLINDRICAL_SURFACE('',#20361,0.425);
#17258=CYLINDRICAL_SURFACE('',#20369,0.24505);
#18100=ADVANCED_FACE('',(#2776),#1990,.T.);
#18101=ADVANCED_FACE('',(#2777),#964,.T.);
#18102=ADVANCED_FACE('',(#2778),#17257,.T.);
#18103=ADVANCED_FACE('',(#2779),#965,.T.);
#18104=ADVANCED_FACE('',(#2780,#1473),#1991,.T.);
#18105=ADVANCED_FACE('',(#2781),#966,.T.);
#18106=ADVANCED_FACE('',(#2782),#17258,.T.);
#18107=ADVANCED_FACE('',(#2783),#967,.T.);
#18108=ADVANCED_FACE('',(#2784),#1992,.T.);
#18109=ADVANCED_FACE('',(#2785),#1993,.F.);
#18110=ADVANCED_FACE('',(#2786),#1994,.F.);
#18111=ADVANCED_FACE('',(#2787),#1995,.F.);
#18112=ADVANCED_FACE('',(#2788),#1996,.F.);
#18113=ADVANCED_FACE('',(#2789),#1997,.F.);
#18114=ADVANCED_FACE('',(#2790),#1998,.F.);
#18115=ADVANCED_FACE('',(#2791),#1999,.F.);
#18116=ADVANCED_FACE('',(#2792),#2000,.F.);
#18595=CLOSED_SHELL('',(#18100,#18101,#18102,#18103,#18104,#18105,#18106,
#18107,#18108));
#18596=CLOSED_SHELL('',(#18109,#18110,#18111,#18112,#18113,#18114,#18115,
#18116));
#20356=AXIS2_PLACEMENT_3D('',#30012,#24247,#24248);
#20357=AXIS2_PLACEMENT_3D('',#30013,#24249,#24250);
#20358=AXIS2_PLACEMENT_3D('',#30015,#24251,#24252);
#20359=AXIS2_PLACEMENT_3D('',#30016,#24253,#24254);
#20360=AXIS2_PLACEMENT_3D('',#30018,#24255,#24256);
#20361=AXIS2_PLACEMENT_3D('',#30020,#24258,#24259);
#20362=AXIS2_PLACEMENT_3D('',#30022,#24260,#24261);
#20363=AXIS2_PLACEMENT_3D('',#30024,#24263,#24264);
#20364=AXIS2_PLACEMENT_3D('',#30026,#24265,#24266);
#20365=AXIS2_PLACEMENT_3D('',#30028,#24268,#24269);
#20366=AXIS2_PLACEMENT_3D('',#30030,#24270,#24271);
#20367=AXIS2_PLACEMENT_3D('',#30031,#24272,#24273);
#20368=AXIS2_PLACEMENT_3D('',#30033,#24274,#24275);
#20369=AXIS2_PLACEMENT_3D('',#30035,#24277,#24278);
#20370=AXIS2_PLACEMENT_3D('',#30037,#24279,#24280);
#20371=AXIS2_PLACEMENT_3D('',#30039,#24282,#24283);
#20372=AXIS2_PLACEMENT_3D('',#30041,#24284,#24285);
#20373=AXIS2_PLACEMENT_3D('',#30043,#24287,#24288);
#20374=AXIS2_PLACEMENT_3D('',#30044,#24289,#24290);
#20375=AXIS2_PLACEMENT_3D('',#30053,#24295,#24296);
#20376=AXIS2_PLACEMENT_3D('',#30059,#24300,#24301);
#20377=AXIS2_PLACEMENT_3D('',#30065,#24305,#24306);
#20378=AXIS2_PLACEMENT_3D('',#30071,#24310,#24311);
#20379=AXIS2_PLACEMENT_3D('',#30077,#24315,#24316);
#20380=AXIS2_PLACEMENT_3D('',#30080,#24319,#24320);
#20381=AXIS2_PLACEMENT_3D('',#30081,#24321,#24322);
#24247=DIRECTION('axis',(0.,0.,1.));
#24248=DIRECTION('refdir',(1.,0.,0.));
#24249=DIRECTION('center_axis',(0.,1.,0.));
#24250=DIRECTION('ref_axis',(0.,0.,1.));
#24251=DIRECTION('center_axis',(0.,-1.,0.));
#24252=DIRECTION('ref_axis',(1.,0.,0.));
#24253=DIRECTION('center_axis',(0.,-1.,0.));
#24254=DIRECTION('ref_axis',(1.,0.,0.));
#24255=DIRECTION('center_axis',(0.,-1.,0.));
#24256=DIRECTION('ref_axis',(1.,0.,0.));
#24257=DIRECTION('',(0.707106781186548,0.707106781186547,8.65956056235493E-17));
#24258=DIRECTION('center_axis',(0.,-1.,0.));
#24259=DIRECTION('ref_axis',(1.,0.,0.));
#24260=DIRECTION('center_axis',(0.,-1.,0.));
#24261=DIRECTION('ref_axis',(1.,0.,0.));
#24262=DIRECTION('',(0.,1.,0.));
#24263=DIRECTION('center_axis',(0.,1.,0.));
#24264=DIRECTION('ref_axis',(1.,0.,0.));
#24265=DIRECTION('center_axis',(0.,-1.,0.));
#24266=DIRECTION('ref_axis',(1.,0.,0.));
#24267=DIRECTION('',(-0.707106781186547,0.707106781186548,-8.65956056235493E-17));
#24268=DIRECTION('center_axis',(0.,-1.,0.));
#24269=DIRECTION('ref_axis',(0.,0.,-1.));
#24270=DIRECTION('center_axis',(0.,-1.,0.));
#24271=DIRECTION('ref_axis',(1.,0.,0.));
#24272=DIRECTION('center_axis',(0.,1.,0.));
#24273=DIRECTION('ref_axis',(1.,0.,0.));
#24274=DIRECTION('center_axis',(0.,1.,0.));
#24275=DIRECTION('ref_axis',(1.,0.,0.));
#24276=DIRECTION('',(-0.447213595499958,0.894427190999916,-5.47678698264203E-17));
#24277=DIRECTION('center_axis',(0.,-1.,0.));
#24278=DIRECTION('ref_axis',(1.,0.,0.));
#24279=DIRECTION('center_axis',(0.,1.,0.));
#24280=DIRECTION('ref_axis',(1.,0.,0.));
#24281=DIRECTION('',(0.,1.,0.));
#24282=DIRECTION('center_axis',(0.,1.,0.));
#24283=DIRECTION('ref_axis',(1.,0.,0.));
#24284=DIRECTION('center_axis',(0.,-1.,0.));
#24285=DIRECTION('ref_axis',(1.,0.,0.));
#24286=DIRECTION('',(-0.707106781186547,0.707106781186548,-8.65956056235493E-17));
#24287=DIRECTION('center_axis',(0.,-1.,0.));
#24288=DIRECTION('ref_axis',(0.,0.,-1.));
#24289=DIRECTION('center_axis',(0.866025403784439,0.,-0.5));
#24290=DIRECTION('ref_axis',(0.5,0.,0.866025403784439));
#24291=DIRECTION('',(-0.5,0.,-0.866025403784439));
#24292=DIRECTION('',(0.,-1.,0.));
#24293=DIRECTION('',(0.5,0.,0.866025403784439));
#24294=DIRECTION('',(0.,-1.,0.));
#24295=DIRECTION('center_axis',(1.20185167898973E-16,0.,-1.));
#24296=DIRECTION('ref_axis',(1.,0.,1.20185167898973E-16));
#24297=DIRECTION('',(-1.,0.,-1.20185167898973E-16));
#24298=DIRECTION('',(0.,-1.,0.));
#24299=DIRECTION('',(1.,0.,1.20185167898973E-16));
#24300=DIRECTION('center_axis',(-0.866025403784439,0.,-0.5));
#24301=DIRECTION('ref_axis',(0.5,0.,-0.866025403784439));
#24302=DIRECTION('',(-0.5,0.,0.866025403784439));
#24303=DIRECTION('',(0.,-1.,0.));
#24304=DIRECTION('',(0.5,0.,-0.866025403784439));
#24305=DIRECTION('center_axis',(-0.866025403784439,0.,0.5));
#24306=DIRECTION('ref_axis',(-0.5,0.,-0.866025403784439));
#24307=DIRECTION('',(0.5,0.,0.866025403784439));
#24308=DIRECTION('',(0.,-1.,0.));
#24309=DIRECTION('',(-0.5,0.,-0.866025403784439));
#24310=DIRECTION('center_axis',(-2.40370335797945E-16,0.,1.));
#24311=DIRECTION('ref_axis',(-1.,0.,-2.40370335797945E-16));
#24312=DIRECTION('',(1.,0.,2.40370335797945E-16));
#24313=DIRECTION('',(0.,-1.,0.));
#24314=DIRECTION('',(-1.,0.,-2.40370335797945E-16));
#24315=DIRECTION('center_axis',(0.866025403784439,0.,0.5));
#24316=DIRECTION('ref_axis',(-0.5,0.,0.866025403784439));
#24317=DIRECTION('',(0.5,0.,-0.866025403784439));
#24318=DIRECTION('',(-0.5,0.,0.866025403784439));
#24319=DIRECTION('center_axis',(0.,1.,0.));
#24320=DIRECTION('ref_axis',(1.,0.,0.));
#24321=DIRECTION('center_axis',(0.,-1.,0.));
#24322=DIRECTION('ref_axis',(0.,0.,-1.));
#30012=CARTESIAN_POINT('',(0.,0.,0.));
#30013=CARTESIAN_POINT('Origin',(0.375,0.5,0.));
#30014=CARTESIAN_POINT('',(-0.375,0.5,-4.59242549680257E-17));
#30015=CARTESIAN_POINT('Origin',(0.,0.5,0.));
#30016=CARTESIAN_POINT('Origin',(0.,0.475,0.));
#30017=CARTESIAN_POINT('',(-0.425,0.45,-5.20474889637625E-17));
#30018=CARTESIAN_POINT('Origin',(0.,0.45,0.));
#30019=CARTESIAN_POINT('',(-0.4,0.475,-4.89858719658941E-17));
#30020=CARTESIAN_POINT('Origin',(0.,0.24,0.));
#30021=CARTESIAN_POINT('',(-0.425,0.0299999999999998,-5.20474889637625E-17));
#30022=CARTESIAN_POINT('Origin',(0.,0.0299999999999998,0.));
#30023=CARTESIAN_POINT('',(-0.425,0.24,-5.20474889637625E-17));
#30024=CARTESIAN_POINT('Origin',(0.,0.0150000000000001,0.));
#30025=CARTESIAN_POINT('',(-0.395,4.85722573273506E-17,-4.83735485663204E-17));
#30026=CARTESIAN_POINT('Origin',(0.,0.,0.));
#30027=CARTESIAN_POINT('',(-0.41,0.0150000000000001,-5.02105187650415E-17));
#30028=CARTESIAN_POINT('Origin',(0.27,0.,0.));
#30029=CARTESIAN_POINT('',(-0.27,0.,-3.30654635769785E-17));
#30030=CARTESIAN_POINT('Origin',(0.,0.,0.));
#30031=CARTESIAN_POINT('Origin',(0.,-0.02,0.));
#30032=CARTESIAN_POINT('',(-0.24505,-0.0498999999999999,3.00099698131059E-17));
#30033=CARTESIAN_POINT('Origin',(0.,-0.0498999999999999,0.));
#30034=CARTESIAN_POINT('',(-0.26,-0.02,-3.18408167778312E-17));
#30035=CARTESIAN_POINT('Origin',(0.,-0.995,0.));
#30036=CARTESIAN_POINT('',(-0.24505,-1.95495,3.00099698131059E-17));
#30037=CARTESIAN_POINT('Origin',(0.,-1.95495,0.));
#30038=CARTESIAN_POINT('',(-0.24505,-0.995,-3.00099698131059E-17));
#30039=CARTESIAN_POINT('Origin',(0.,-1.975,0.));
#30040=CARTESIAN_POINT('',(-0.2,-2.,-2.44929359829471E-17));
#30041=CARTESIAN_POINT('Origin',(0.,-2.,0.));
#30042=CARTESIAN_POINT('',(-0.225,-1.975,-2.75545529808154E-17));
#30043=CARTESIAN_POINT('Origin',(0.,-2.,0.));
#30044=CARTESIAN_POINT('Origin',(0.115470053837925,-0.5,-0.2));
#30045=CARTESIAN_POINT('',(0.23094010767585,-0.5,0.));
#30046=CARTESIAN_POINT('',(0.115470053837925,-0.5,-0.2));
#30047=CARTESIAN_POINT('',(0.23094010767585,-0.5,0.));
#30048=CARTESIAN_POINT('',(0.115470053837925,-0.8,-0.2));
#30049=CARTESIAN_POINT('',(0.115470053837925,-0.5,-0.2));
#30050=CARTESIAN_POINT('',(0.23094010767585,-0.8,0.));
#30051=CARTESIAN_POINT('',(0.23094010767585,-0.8,0.));
#30052=CARTESIAN_POINT('',(0.23094010767585,-0.5,0.));
#30053=CARTESIAN_POINT('Origin',(-0.115470053837925,-0.5,-0.2));
#30054=CARTESIAN_POINT('',(-0.115470053837925,-0.5,-0.2));
#30055=CARTESIAN_POINT('',(0.115470053837925,-0.5,-0.2));
#30056=CARTESIAN_POINT('',(-0.115470053837925,-0.8,-0.2));
#30057=CARTESIAN_POINT('',(-0.115470053837925,-0.5,-0.2));
#30058=CARTESIAN_POINT('',(0.115470053837925,-0.8,-0.2));
#30059=CARTESIAN_POINT('Origin',(-0.23094010767585,-0.5,-2.77555756156289E-17));
#30060=CARTESIAN_POINT('',(-0.23094010767585,-0.5,-2.82820063659975E-17));
#30061=CARTESIAN_POINT('',(-0.115470053837925,-0.5,-0.2));
#30062=CARTESIAN_POINT('',(-0.23094010767585,-0.8,-2.77555756156289E-17));
#30063=CARTESIAN_POINT('',(-0.23094010767585,-0.5,-2.82820063659975E-17));
#30064=CARTESIAN_POINT('',(-0.115470053837925,-0.8,-0.2));
#30065=CARTESIAN_POINT('Origin',(-0.115470053837925,-0.5,0.2));
#30066=CARTESIAN_POINT('',(-0.115470053837925,-0.5,0.2));
#30067=CARTESIAN_POINT('',(-0.23094010767585,-0.5,-2.82820063659975E-17));
#30068=CARTESIAN_POINT('',(-0.115470053837925,-0.8,0.2));
#30069=CARTESIAN_POINT('',(-0.115470053837925,-0.5,0.2));
#30070=CARTESIAN_POINT('',(-0.23094010767585,-0.8,-2.82820063659975E-17));
#30071=CARTESIAN_POINT('Origin',(0.115470053837925,-0.5,0.2));
#30072=CARTESIAN_POINT('',(0.115470053837925,-0.5,0.2));
#30073=CARTESIAN_POINT('',(-0.115470053837925,-0.5,0.2));
#30074=CARTESIAN_POINT('',(0.115470053837925,-0.8,0.2));
#30075=CARTESIAN_POINT('',(0.115470053837925,-0.5,0.2));
#30076=CARTESIAN_POINT('',(-0.115470053837925,-0.8,0.2));
#30077=CARTESIAN_POINT('Origin',(0.23094010767585,-0.5,0.));
#30078=CARTESIAN_POINT('',(0.115470053837925,-0.5,0.2));
#30079=CARTESIAN_POINT('',(0.115470053837925,-0.8,0.2));
#30080=CARTESIAN_POINT('Origin',(0.,-0.5,0.));
#30081=CARTESIAN_POINT('Origin',(0.,-0.8,0.));
#43426=UNCERTAINTY_MEASURE_WITH_UNIT(LENGTH_MEASURE(0.001),#43522,
'DISTANCE_ACCURACY_VALUE',
'Maximum model space distance between geometric entities at asserted c
onnectivities');
#43453=UNCERTAINTY_MEASURE_WITH_UNIT(LENGTH_MEASURE(0.001),#43522,
'DISTANCE_ACCURACY_VALUE',
'Maximum model space distance between geometric entities at asserted c
onnectivities');
#43494=(
GEOMETRIC_REPRESENTATION_CONTEXT(3)
GLOBAL_UNCERTAINTY_ASSIGNED_CONTEXT((#43426))
GLOBAL_UNIT_ASSIGNED_CONTEXT((#43522,#43524,#43525))
REPRESENTATION_CONTEXT('','3D')
);
#43521=(
GEOMETRIC_REPRESENTATION_CONTEXT(3)
GLOBAL_UNCERTAINTY_ASSIGNED_CONTEXT((#43453))
GLOBAL_UNIT_ASSIGNED_CONTEXT((#43522,#43524,#43525))
REPRESENTATION_CONTEXT('','3D')
);
#43522=(
LENGTH_UNIT()
NAMED_UNIT(*)
SI_UNIT(.CENTI.,.METRE.)
);
#43524=(
NAMED_UNIT(*)
PLANE_ANGLE_UNIT()
SI_UNIT($,.RADIAN.)
);
#43525=(
NAMED_UNIT(*)
SI_UNIT($,.STERADIAN.)
SOLID_ANGLE_UNIT()
);
#43566=SHAPE_DEFINITION_REPRESENTATION(#43643,#43834);
#43643=PRODUCT_DEFINITION_SHAPE('',$,#43902);
#43834=SHAPE_REPRESENTATION('',(#20356),#43494);
#43861=PRODUCT_DEFINITION_CONTEXT('part definition',#44064,'design');
#43902=PRODUCT_DEFINITION('Cap Screw - M5x20','Cap Screw - M5x20',#43969,
#43861);
#43969=PRODUCT_DEFINITION_FORMATION('',$,#44106);
#44064=APPLICATION_CONTEXT(
'Core Data for Automotive Mechanical Design Process');
#44065=PRODUCT_CONTEXT('part definition',#44064,'mechanical');
#44106=PRODUCT('Cap Screw - M5x20','Cap Screw - M5x20',
'Cap Screw - M5x20',(#44065));
#44203=COLOUR_RGB('Black',0.12,0.14,0.17);
#44204=FILL_AREA_STYLE_COLOUR('',#44203);
#44205=FILL_AREA_STYLE('',(#44204));
#44206=SURFACE_STYLE_FILL_AREA(#44205);
#44207=SURFACE_SIDE_STYLE('',(#44206));
#44208=SURFACE_STYLE_USAGE(.BOTH.,#44207);
#44209=PRESENTATION_STYLE_ASSIGNMENT((#44208));
ENDSEC;
END-ISO-10303-21;
